ISO-10303-21;
HEADER;
FILE_DESCRIPTION (('STEP AP214'),
    '1' );
FILE_NAME ('Cylinder Alignment Washers.step',
    '2026-10-09T09:51:18',
    ( '' ),
    ( '' ),
    'SwSTEP 2.0',
    'SolidWorks 2026',
    '' );
FILE_SCHEMA (( 'AUTOMOTIVE_DESIGN' ));
ENDSEC;

DATA;
#7=EDGE_CURVE ( 'NONE', #38833, #36313, #30041, .T. ) ;
#20=DIRECTION ( 'NONE',  ( -1.927470528863183637E-16, -1.434740771370715221E-29, 1.000000000000000000 ) ) ;
#203=DIRECTION ( 'NONE',  ( 1.927470528863184130E-16, 1.434740771370715221E-29, -1.000000000000000000 ) ) ;
#262=DIRECTION ( 'NONE',  ( 1.000000000000000000, 0.000000000000000000, 0.000000000000000000 ) ) ;
#390=CARTESIAN_POINT ( 'NONE',  ( -19.92409385541305156, -14.80920654474411080, 47.99999999999997868 ) ) ;
#479=CARTESIAN_POINT ( 'NONE',  ( -17.02409385541305298, -14.80920654474411080, 47.99999999999997868 ) ) ;
#634=DIRECTION ( 'NONE',  ( -1.927470528863183637E-16, -1.434740771370715221E-29, 1.000000000000000000 ) ) ;
#689=CARTESIAN_POINT ( 'NONE',  ( -17.02409385541305298, -14.80920654474411080, 47.99999999999997868 ) ) ;
#1014=DIRECTION ( 'NONE',  ( 1.927470528863184130E-16, 1.434740771370715221E-29, -1.000000000000000000 ) ) ;
#1054=ORIENTED_EDGE ( 'NONE', *, *, #36056, .T. ) ;
#1171=AXIS2_PLACEMENT_3D ( 'NONE', #7204, #36702, #10640 ) ;
#1276=CARTESIAN_POINT ( 'NONE',  ( -17.42409385541305511, -14.80920654474411080, 47.99999999999997868 ) ) ;
#1696=( NAMED_UNIT ( * ) SI_UNIT ( $, .STERADIAN. ) SOLID_ANGLE_UNIT ( ) );
#3195=CARTESIAN_POINT ( 'NONE',  ( -19.92409385541305866, -14.80920654474411080, 75.49999999999998579 ) ) ;
#3232=AXIS2_PLACEMENT_3D ( 'NONE', #3704, #20, #15003 ) ;
#3270=( GEOMETRIC_REPRESENTATION_CONTEXT ( 3 ) GLOBAL_UNCERTAINTY_ASSIGNED_CONTEXT ( ( #31222 ) ) GLOBAL_UNIT_ASSIGNED_CONTEXT ( ( #11692, #16758, #26959 ) ) REPRESENTATION_CONTEXT ( 'NONE', 'WORKASPACE' ) );
#3704=CARTESIAN_POINT ( 'NONE',  ( -17.42409385541306222, -15.20920654474411116, 75.49999999999998579 ) ) ;
#3742=DIRECTION ( 'NONE',  ( 1.000000000000000000, 0.000000000000000000, 0.000000000000000000 ) ) ;
#3813=FACE_OUTER_BOUND ( 'NONE', #10196, .T. ) ;
#4002=AXIS2_PLACEMENT_3D ( 'NONE', #42528, #203, #45260 ) ;
#4012=ORIENTED_EDGE ( 'NONE', *, *, #29262, .F. ) ;
#4277=ADVANCED_FACE ( 'NONE', ( #23719 ), #31570, .T. ) ;
#4536=APPLICATION_CONTEXT ( 'automotive_design' ) ;
#4961=CARTESIAN_POINT ( 'NONE',  ( -14.92409385541305333, -14.80920654474411080, 47.99999999999997868 ) ) ;
#5069=SHAPE_DEFINITION_REPRESENTATION ( #7948, #5940 ) ;
#5665=ORIENTED_EDGE ( 'NONE', *, *, #13423, .F. ) ;
#5940=SHAPE_REPRESENTATION ( 'Cylinder Alignment Washers', ( #29031 ), #10942 ) ;
#6103=CARTESIAN_POINT ( 'NONE',  ( -14.92409385541306044, -14.80920654474411080, 75.49999999999998579 ) ) ;
#6150=EDGE_LOOP ( 'NONE', ( #26876, #22920 ) ) ;
#6397=STYLED_ITEM ( 'NONE', ( #20485 ), #31806 ) ;
#6534=VECTOR ( 'NONE', #30679, 1000.000000000000000 ) ;
#6589=LINE ( 'NONE', #28270, #31194 ) ;
#6950=DIRECTION ( 'NONE',  ( 1.000000000000000000, 0.000000000000000000, 0.000000000000000000 ) ) ;
#7003=PRODUCT_DEFINITION_FORMATION_WITH_SPECIFIED_SOURCE ( 'ANY', '', #38600, .NOT_KNOWN. ) ;
#7204=CARTESIAN_POINT ( 'NONE',  ( -17.42409385541306222, -14.80920654474411080, 82.49999999999998579 ) ) ;
#7318=ORIENTED_EDGE ( 'NONE', *, *, #37904, .T. ) ;
#7650=DIRECTION ( 'NONE',  ( 1.927470528863184130E-16, 1.434740771370715221E-29, -1.000000000000000000 ) ) ;
#7769=ORIENTED_EDGE ( 'NONE', *, *, #8538, .F. ) ;
#7948=PRODUCT_DEFINITION_SHAPE ( 'NONE', 'NONE',  #9035 ) ;
#8245=CYLINDRICAL_SURFACE ( 'NONE', #13389, 0.4000000000000010214 ) ;
#8538=EDGE_CURVE ( 'NONE', #12573, #38501, #38175, .T. ) ;
#8861=DIRECTION ( 'NONE',  ( 1.000000000000000000, 1.665334536937734564E-16, 1.927470528863183637E-16 ) ) ;
#9035=PRODUCT_DEFINITION ( 'UNKNOWN', '', #7003, #32670 ) ;
#9068=ORIENTED_EDGE ( 'NONE', *, *, #8538, .T. ) ;
#9163=CARTESIAN_POINT ( 'NONE',  ( -14.92409385541306044, -14.80920654474411080, 82.49999999999998579 ) ) ;
#9339=CIRCLE ( 'NONE', #15603, 0.4000000000000010214 ) ;
#9562=VERTEX_POINT ( 'NONE', #43816 ) ;
#9592=PLANE ( 'NONE',  #17784 ) ;
#9784=DIRECTION ( 'NONE',  ( 1.000000000000000000, 0.000000000000000000, 0.000000000000000000 ) ) ;
#9993=AXIS2_PLACEMENT_3D ( 'NONE', #16022, #15047, #3742 ) ;
#10041=DIRECTION ( 'NONE',  ( 1.927470528863184130E-16, 1.434740771370715221E-29, -1.000000000000000000 ) ) ;
#10189=ADVANCED_FACE ( 'NONE', ( #3813 ), #8245, .T. ) ;
#10196=EDGE_LOOP ( 'NONE', ( #5665, #19156, #28775, #27809 ) ) ;
#10218=DIRECTION ( 'NONE',  ( 1.927470528863184130E-16, 1.434740771370715221E-29, -1.000000000000000000 ) ) ;
#10230=ORIENTED_EDGE ( 'NONE', *, *, #33305, .T. ) ;
#10341=AXIS2_PLACEMENT_3D ( 'NONE', #18210, #7650, #262 ) ;
#10600=EDGE_LOOP ( 'NONE', ( #47121, #29554 ) ) ;
#10640=DIRECTION ( 'NONE',  ( 1.000000000000000000, 0.000000000000000000, 0.000000000000000000 ) ) ;
#10803=EDGE_CURVE ( 'NONE', #32331, #36313, #29152, .T. ) ;
#10942=( GEOMETRIC_REPRESENTATION_CONTEXT ( 3 ) GLOBAL_UNCERTAINTY_ASSIGNED_CONTEXT ( ( #46008 ) ) GLOBAL_UNIT_ASSIGNED_CONTEXT ( ( #31734, #46525, #1696 ) ) REPRESENTATION_CONTEXT ( 'NONE', 'WORKASPACE' ) );
#11096=PLANE ( 'NONE',  #3232 ) ;
#11692=( LENGTH_UNIT ( ) NAMED_UNIT ( * ) SI_UNIT ( .MILLI., .METRE. ) );
#11717=DIRECTION ( 'NONE',  ( -1.000000000000000000, -1.665334536937734564E-16, -1.927470528863183637E-16 ) ) ;
#11729=DIRECTION ( 'NONE',  ( 1.927470528863184130E-16, 1.434740771370715221E-29, -1.000000000000000000 ) ) ;
#11946=SURFACE_STYLE_FILL_AREA ( #45437 ) ;
#12094=APPLICATION_CONTEXT ( 'automotive_design' ) ;
#12170=DIRECTION ( 'NONE',  ( 1.000000000000000000, 0.000000000000000000, 0.000000000000000000 ) ) ;
#12573=VERTEX_POINT ( 'NONE', #9163 ) ;
#13161=ORIENTED_EDGE ( 'NONE', *, *, #20956, .T. ) ;
#13389=AXIS2_PLACEMENT_3D ( 'NONE', #37272, #22783, #12170 ) ;
#13419=CIRCLE ( 'NONE', #23688, 0.4000000000000010214 ) ;
#13423=EDGE_CURVE ( 'NONE', #28434, #32331, #6589, .T. ) ;
#13952=EDGE_CURVE ( 'NONE', #12573, #9562, #25731, .T. ) ;
#14024=FACE_OUTER_BOUND ( 'NONE', #25566, .T. ) ;
#14267=FACE_BOUND ( 'NONE', #18614, .T. ) ;
#14645=CARTESIAN_POINT ( 'NONE',  ( -17.42409385541306222, -14.80920654474411080, 75.49999999999998579 ) ) ;
#14937=CLOSED_SHELL ( 'NONE', ( #4277, #28164, #24746, #10189, #21404, #37042, #42174 ) ) ;
#15003=DIRECTION ( 'NONE',  ( -1.000000000000000000, -1.665334536937734564E-16, -1.927470528863183637E-16 ) ) ;
#15047=DIRECTION ( 'NONE',  ( 1.927470528863184130E-16, 1.434740771370715221E-29, -1.000000000000000000 ) ) ;
#15603=AXIS2_PLACEMENT_3D ( 'NONE', #47637, #10218, #28678 ) ;
#16022=CARTESIAN_POINT ( 'NONE',  ( -17.42409385541306222, -14.80920654474411080, 82.49999999999998579 ) ) ;
#16365=FACE_OUTER_BOUND ( 'NONE', #6150, .T. ) ;
#16758=( NAMED_UNIT ( * ) PLANE_ANGLE_UNIT ( ) SI_UNIT ( $, .RADIAN. ) );
#17170=SHAPE_REPRESENTATION_RELATIONSHIP ( 'NONE' , 'NONE' ,  #5940, #28519 ) ;
#17784=AXIS2_PLACEMENT_3D ( 'NONE', #42601, #20901, #8861 ) ;
#17936=DIRECTION ( 'NONE',  ( 1.927470528863184130E-16, 1.434740771370715221E-29, -1.000000000000000000 ) ) ;
#18210=CARTESIAN_POINT ( 'NONE',  ( -17.42409385541306222, -14.80920654474411080, 75.49999999999998579 ) ) ;
#18254=DIRECTION ( 'NONE',  ( 1.927470528863184130E-16, 1.434740771370715221E-29, -1.000000000000000000 ) ) ;
#18614=EDGE_LOOP ( 'NONE', ( #35236, #4012 ) ) ;
#18653=EDGE_LOOP ( 'NONE', ( #19887, #10230, #19608, #7769 ) ) ;
#18722=AXIS2_PLACEMENT_3D ( 'NONE', #45460, #634, #11717 ) ;
#18988=EDGE_LOOP ( 'NONE', ( #29311, #1054, #9068, #33741 ) ) ;
#19156=ORIENTED_EDGE ( 'NONE', *, *, #29262, .T. ) ;
#19608=ORIENTED_EDGE ( 'NONE', *, *, #31988, .F. ) ;
#19887=ORIENTED_EDGE ( 'NONE', *, *, #13952, .T. ) ;
#20184=ORIENTED_EDGE ( 'NONE', *, *, #31988, .T. ) ;
#20485=PRESENTATION_STYLE_ASSIGNMENT (( #23514 ) ) ;
#20901=DIRECTION ( 'NONE',  ( 1.927470528863183637E-16, 1.434740771370715221E-29, -1.000000000000000000 ) ) ;
#20956=EDGE_CURVE ( 'NONE', #38833, #28434, #13419, .T. ) ;
#21340=MECHANICAL_DESIGN_GEOMETRIC_PRESENTATION_REPRESENTATION('',(#6397),#3270);
#21404=ADVANCED_FACE ( 'NONE', ( #14267, #14024 ), #11096, .F. ) ;
#21654=FACE_OUTER_BOUND ( 'NONE', #18988, .T. ) ;
#22089=ORIENTED_EDGE ( 'NONE', *, *, #7, .F. ) ;
#22783=DIRECTION ( 'NONE',  ( 1.927470528863184130E-16, 1.434740771370715221E-29, -1.000000000000000000 ) ) ;
#22920=ORIENTED_EDGE ( 'NONE', *, *, #10803, .T. ) ;
#23514=SURFACE_STYLE_USAGE ( .BOTH. , #26467 ) ;
#23688=AXIS2_PLACEMENT_3D ( 'NONE', #25449, #35553, #36027 ) ;
#23719=FACE_OUTER_BOUND ( 'NONE', #18653, .T. ) ;
#24746=ADVANCED_FACE ( 'NONE', ( #16365 ), #34348, .F. ) ;
#25281=FACE_OUTER_BOUND ( 'NONE', #41099, .T. ) ;
#25449=CARTESIAN_POINT ( 'NONE',  ( -17.42409385541306222, -14.80920654474411080, 75.49999999999998579 ) ) ;
#25512=DIRECTION ( 'NONE',  ( 1.927470528863184130E-16, 1.434740771370715221E-29, -1.000000000000000000 ) ) ;
#25566=EDGE_LOOP ( 'NONE', ( #20184, #7318 ) ) ;
#25731=CIRCLE ( 'NONE', #9993, 2.500000000000000444 ) ;
#25737=AXIS2_PLACEMENT_3D ( 'NONE', #1276, #31085, #42173 ) ;
#26467=SURFACE_SIDE_STYLE ('',( #11946 ) ) ;
#26876=ORIENTED_EDGE ( 'NONE', *, *, #45699, .T. ) ;
#26959=( NAMED_UNIT ( * ) SI_UNIT ( $, .STERADIAN. ) SOLID_ANGLE_UNIT ( ) );
#27080=CIRCLE ( 'NONE', #38076, 2.500000000000000444 ) ;
#27560=FACE_OUTER_BOUND ( 'NONE', #10600, .T. ) ;
#27809=ORIENTED_EDGE ( 'NONE', *, *, #10803, .F. ) ;
#28164=ADVANCED_FACE ( 'NONE', ( #25281 ), #28493, .T. ) ;
#28270=CARTESIAN_POINT ( 'NONE',  ( -17.82409385541305724, -14.80920654474411080, 47.99999999999997868 ) ) ;
#28434=VERTEX_POINT ( 'NONE', #42735 ) ;
#28493=CYLINDRICAL_SURFACE ( 'NONE', #30738, 0.4000000000000010214 ) ;
#28519=ADVANCED_BREP_SHAPE_REPRESENTATION ( '', ( #31806, #29031 ), #10942 ) ;
#28678=DIRECTION ( 'NONE',  ( 1.000000000000000000, 0.000000000000000000, 0.000000000000000000 ) ) ;
#28775=ORIENTED_EDGE ( 'NONE', *, *, #7, .T. ) ;
#29031=AXIS2_PLACEMENT_3D ( 'NONE', #29301, #44568, #33698 ) ;
#29111=CARTESIAN_POINT ( 'NONE',  ( -17.42409385541306222, -14.80920654474411080, 75.49999999999998579 ) ) ;
#29152=CIRCLE ( 'NONE', #4002, 0.4000000000000010214 ) ;
#29202=COLOUR_RGB ( '', 0.40784314, 0.44705882, 0.49803922) ;
#29262=EDGE_CURVE ( 'NONE', #28434, #38833, #40990, .T. ) ;
#29301=CARTESIAN_POINT ( 'NONE',  ( 0.000000000000000000, 0.000000000000000000, 0.000000000000000000 ) ) ;
#29311=ORIENTED_EDGE ( 'NONE', *, *, #33305, .F. ) ;
#29463=ORIENTED_EDGE ( 'NONE', *, *, #13423, .T. ) ;
#29554=ORIENTED_EDGE ( 'NONE', *, *, #36056, .F. ) ;
#30041=LINE ( 'NONE', #479, #33859 ) ;
#30179=FILL_AREA_STYLE_COLOUR ( '', #29202 ) ;
#30679=DIRECTION ( 'NONE',  ( 1.927470528863184130E-16, 1.434740771370715221E-29, -1.000000000000000000 ) ) ;
#30738=AXIS2_PLACEMENT_3D ( 'NONE', #36343, #25512, #9784 ) ;
#31085=DIRECTION ( 'NONE',  ( 1.927470528863184130E-16, 1.434740771370715221E-29, -1.000000000000000000 ) ) ;
#31194=VECTOR ( 'NONE', #10041, 1000.000000000000000 ) ;
#31222=UNCERTAINTY_MEASURE_WITH_UNIT (LENGTH_MEASURE( 1.000000000000000082E-05 ), #11692, 'distance_accuracy_value', 'NONE');
#31570=CYLINDRICAL_SURFACE ( 'NONE', #25737, 2.500000000000000444 ) ;
#31734=( LENGTH_UNIT ( ) NAMED_UNIT ( * ) SI_UNIT ( .MILLI., .METRE. ) );
#31806=MANIFOLD_SOLID_BREP ( 'Stock-MAS-175-1', #14937 ) ;
#31988=EDGE_CURVE ( 'NONE', #38501, #40815, #43385, .T. ) ;
#32331=VERTEX_POINT ( 'NONE', #44525 ) ;
#32670=PRODUCT_DEFINITION_CONTEXT ( 'detailed design', #12094, 'design' ) ;
#33305=EDGE_CURVE ( 'NONE', #9562, #40815, #38774, .T. ) ;
#33380=CIRCLE ( 'NONE', #1171, 2.500000000000000444 ) ;
#33618=DIRECTION ( 'NONE',  ( 1.000000000000000000, 0.000000000000000000, 0.000000000000000000 ) ) ;
#33698=DIRECTION ( 'NONE',  ( 1.000000000000000000, 0.000000000000000000, 0.000000000000000000 ) ) ;
#33741=ORIENTED_EDGE ( 'NONE', *, *, #37904, .F. ) ;
#33859=VECTOR ( 'NONE', #37893, 1000.000000000000000 ) ;
#34348=PLANE ( 'NONE',  #18722 ) ;
#35236=ORIENTED_EDGE ( 'NONE', *, *, #20956, .F. ) ;
#35553=DIRECTION ( 'NONE',  ( 1.927470528863184130E-16, 1.434740771370715221E-29, -1.000000000000000000 ) ) ;
#36027=DIRECTION ( 'NONE',  ( 1.000000000000000000, 0.000000000000000000, 0.000000000000000000 ) ) ;
#36056=EDGE_CURVE ( 'NONE', #9562, #12573, #33380, .T. ) ;
#36137=VECTOR ( 'NONE', #1014, 1000.000000000000000 ) ;
#36313=VERTEX_POINT ( 'NONE', #689 ) ;
#36343=CARTESIAN_POINT ( 'NONE',  ( -17.42409385541305511, -14.80920654474411080, 47.99999999999997868 ) ) ;
#36702=DIRECTION ( 'NONE',  ( 1.927470528863184130E-16, 1.434740771370715221E-29, -1.000000000000000000 ) ) ;
#37042=ADVANCED_FACE ( 'NONE', ( #21654 ), #47285, .T. ) ;
#37272=CARTESIAN_POINT ( 'NONE',  ( -17.42409385541305511, -14.80920654474411080, 47.99999999999997868 ) ) ;
#37893=DIRECTION ( 'NONE',  ( 1.927470528863184130E-16, 1.434740771370715221E-29, -1.000000000000000000 ) ) ;
#37904=EDGE_CURVE ( 'NONE', #40815, #38501, #27080, .T. ) ;
#38076=AXIS2_PLACEMENT_3D ( 'NONE', #29111, #18254, #6950 ) ;
#38175=LINE ( 'NONE', #4961, #36137 ) ;
#38501=VERTEX_POINT ( 'NONE', #6103 ) ;
#38600=PRODUCT ( 'Cylinder Alignment Washers', 'Cylinder Alignment Washers', '', ( #42005 ) ) ;
#38774=LINE ( 'NONE', #390, #6534 ) ;
#38833=VERTEX_POINT ( 'NONE', #48309 ) ;
#40368=CARTESIAN_POINT ( 'NONE',  ( -17.42409385541305511, -14.80920654474411080, 47.99999999999997868 ) ) ;
#40815=VERTEX_POINT ( 'NONE', #3195 ) ;
#40990=CIRCLE ( 'NONE', #47289, 0.4000000000000010214 ) ;
#41099=EDGE_LOOP ( 'NONE', ( #13161, #29463, #45966, #22089 ) ) ;
#41989=AXIS2_PLACEMENT_3D ( 'NONE', #40368, #17936, #47753 ) ;
#42005=PRODUCT_CONTEXT ( 'NONE', #4536, 'mechanical' ) ;
#42173=DIRECTION ( 'NONE',  ( 1.000000000000000000, 0.000000000000000000, 0.000000000000000000 ) ) ;
#42174=ADVANCED_FACE ( 'NONE', ( #27560 ), #9592, .F. ) ;
#42528=CARTESIAN_POINT ( 'NONE',  ( -17.42409385541305511, -14.80920654474411080, 47.99999999999997868 ) ) ;
#42601=CARTESIAN_POINT ( 'NONE',  ( -17.42409385541306222, -17.30920654474411080, 82.49999999999998579 ) ) ;
#42735=CARTESIAN_POINT ( 'NONE',  ( -17.82409385541306079, -14.80920654474411080, 75.49999999999998579 ) ) ;
#43385=CIRCLE ( 'NONE', #10341, 2.500000000000000444 ) ;
#43816=CARTESIAN_POINT ( 'NONE',  ( -19.92409385541305866, -14.80920654474411080, 82.49999999999998579 ) ) ;
#44525=CARTESIAN_POINT ( 'NONE',  ( -17.82409385541305724, -14.80920654474411080, 47.99999999999997868 ) ) ;
#44568=DIRECTION ( 'NONE',  ( 0.000000000000000000, 0.000000000000000000, 1.000000000000000000 ) ) ;
#45260=DIRECTION ( 'NONE',  ( 1.000000000000000000, 0.000000000000000000, 0.000000000000000000 ) ) ;
#45437=FILL_AREA_STYLE ('',( #30179 ) ) ;
#45460=CARTESIAN_POINT ( 'NONE',  ( -17.42409385541305511, -14.80920654474411080, 47.99999999999997868 ) ) ;
#45699=EDGE_CURVE ( 'NONE', #36313, #32331, #9339, .T. ) ;
#45966=ORIENTED_EDGE ( 'NONE', *, *, #45699, .F. ) ;
#46008=UNCERTAINTY_MEASURE_WITH_UNIT (LENGTH_MEASURE( 1.000000000000000082E-05 ), #31734, 'distance_accuracy_value', 'NONE');
#46525=( NAMED_UNIT ( * ) PLANE_ANGLE_UNIT ( ) SI_UNIT ( $, .RADIAN. ) );
#47121=ORIENTED_EDGE ( 'NONE', *, *, #13952, .F. ) ;
#47285=CYLINDRICAL_SURFACE ( 'NONE', #41989, 2.500000000000000444 ) ;
#47289=AXIS2_PLACEMENT_3D ( 'NONE', #14645, #11729, #33618 ) ;
#47637=CARTESIAN_POINT ( 'NONE',  ( -17.42409385541305511, -14.80920654474411080, 47.99999999999997868 ) ) ;
#47753=DIRECTION ( 'NONE',  ( 1.000000000000000000, 0.000000000000000000, 0.000000000000000000 ) ) ;
#48309=CARTESIAN_POINT ( 'NONE',  ( -17.02409385541306008, -14.80920654474411080, 75.49999999999998579 ) ) ;
ENDSEC;
END-ISO-10303-21;
